ISO-10303-21;
HEADER;
/* Generated by software containing ST-Developer
 * from STEP Tools, Inc. (www.steptools.com) 
 */

FILE_DESCRIPTION(
/* description */ ('Twin-shackle spreader bar'),
/* implementation_level */ '2;1');

FILE_NAME(
/* name */ 'Flat Washer - M10.step',
/* time_stamp */ '2026-10-27T20:18:10-07:00',
/* author */ (''),
/* organization */ (''),
/* preprocessor_version */ 'ST-DEVELOPER v20.2',
/* originating_system */ 'Autodesk Translation Framework v15.17.0.0',
/* authorisation */ '');

FILE_SCHEMA (('AUTOMOTIVE_DESIGN { 1 0 10303 214 3 1 1 }'));
ENDSEC;

DATA;
#10=MECHANICAL_DESIGN_GEOMETRIC_PRESENTATION_REPRESENTATION('',(#162),#1829);
#122=CIRCLE('',#1096,0.525);
#123=CIRCLE('',#1097,0.525);
#124=CIRCLE('',#1099,1.);
#125=CIRCLE('',#1100,1.);
#140=CYLINDRICAL_SURFACE('',#1095,0.525);
#141=CYLINDRICAL_SURFACE('',#1098,1.);
#148=SHAPE_REPRESENTATION_RELATIONSHIP('SRR','None',#1886,#155);
#155=ADVANCED_BREP_SHAPE_REPRESENTATION('',(#169),#1827);
#162=STYLED_ITEM('',(#1991),#169);
#169=MANIFOLD_SOLID_BREP('Body1',#942);
#183=FACE_BOUND('',#292,.T.);
#184=FACE_BOUND('',#294,.T.);
#227=FACE_OUTER_BOUND('',#289,.T.);
#228=FACE_OUTER_BOUND('',#290,.T.);
#229=FACE_OUTER_BOUND('',#291,.T.);
#230=FACE_OUTER_BOUND('',#293,.T.);
#289=EDGE_LOOP('',(#816,#817,#818,#819));
#290=EDGE_LOOP('',(#820,#821,#822,#823));
#291=EDGE_LOOP('',(#824));
#292=EDGE_LOOP('',(#825));
#293=EDGE_LOOP('',(#826));
#294=EDGE_LOOP('',(#827));
#370=LINE('',#1703,#446);
#371=LINE('',#1709,#447);
#446=VECTOR('',#1350,0.525);
#447=VECTOR('',#1357,1.);
#513=VERTEX_POINT('',#1700);
#514=VERTEX_POINT('',#1702);
#515=VERTEX_POINT('',#1706);
#516=VERTEX_POINT('',#1708);
#616=EDGE_CURVE('',#513,#513,#122,.T.);
#617=EDGE_CURVE('',#513,#514,#370,.T.);
#618=EDGE_CURVE('',#514,#514,#123,.T.);
#619=EDGE_CURVE('',#515,#515,#124,.T.);
#620=EDGE_CURVE('',#515,#516,#371,.T.);
#621=EDGE_CURVE('',#516,#516,#125,.T.);
#816=ORIENTED_EDGE('',*,*,#616,.F.);
#817=ORIENTED_EDGE('',*,*,#617,.T.);
#818=ORIENTED_EDGE('',*,*,#618,.T.);
#819=ORIENTED_EDGE('',*,*,#617,.F.);
#820=ORIENTED_EDGE('',*,*,#619,.F.);
#821=ORIENTED_EDGE('',*,*,#620,.T.);
#822=ORIENTED_EDGE('',*,*,#621,.T.);
#823=ORIENTED_EDGE('',*,*,#620,.F.);
#824=ORIENTED_EDGE('',*,*,#619,.T.);
#825=ORIENTED_EDGE('',*,*,#616,.T.);
#826=ORIENTED_EDGE('',*,*,#621,.F.);
#827=ORIENTED_EDGE('',*,*,#618,.F.);
#882=PLANE('',#1101);
#883=PLANE('',#1102);
#928=ADVANCED_FACE('',(#227),#140,.F.);
#929=ADVANCED_FACE('',(#228),#141,.T.);
#930=ADVANCED_FACE('',(#229,#183),#882,.T.);
#931=ADVANCED_FACE('',(#230,#184),#883,.F.);
#942=CLOSED_SHELL('',(#928,#929,#930,#931));
#1094=AXIS2_PLACEMENT_3D('',#1698,#1344,#1345);
#1095=AXIS2_PLACEMENT_3D('',#1699,#1346,#1347);
#1096=AXIS2_PLACEMENT_3D('',#1701,#1348,#1349);
#1097=AXIS2_PLACEMENT_3D('',#1704,#1351,#1352);
#1098=AXIS2_PLACEMENT_3D('',#1705,#1353,#1354);
#1099=AXIS2_PLACEMENT_3D('',#1707,#1355,#1356);
#1100=AXIS2_PLACEMENT_3D('',#1710,#1358,#1359);
#1101=AXIS2_PLACEMENT_3D('',#1711,#1360,#1361);
#1102=AXIS2_PLACEMENT_3D('',#1712,#1362,#1363);
#1344=DIRECTION('axis',(0.,0.,1.));
#1345=DIRECTION('refdir',(1.,0.,0.));
#1346=DIRECTION('center_axis',(0.,1.,0.));
#1347=DIRECTION('ref_axis',(1.,0.,0.));
#1348=DIRECTION('center_axis',(0.,-1.,0.));
#1349=DIRECTION('ref_axis',(1.,0.,0.));
#1350=DIRECTION('',(0.,-1.,0.));
#1351=DIRECTION('center_axis',(0.,-1.,0.));
#1352=DIRECTION('ref_axis',(1.,0.,0.));
#1353=DIRECTION('center_axis',(0.,1.,0.));
#1354=DIRECTION('ref_axis',(1.,0.,0.));
#1355=DIRECTION('center_axis',(0.,1.,0.));
#1356=DIRECTION('ref_axis',(1.,0.,0.));
#1357=DIRECTION('',(0.,-1.,0.));
#1358=DIRECTION('center_axis',(0.,1.,0.));
#1359=DIRECTION('ref_axis',(1.,0.,0.));
#1360=DIRECTION('center_axis',(0.,1.,0.));
#1361=DIRECTION('ref_axis',(1.,0.,0.));
#1362=DIRECTION('center_axis',(0.,1.,0.));
#1363=DIRECTION('ref_axis',(1.,0.,0.));
#1698=CARTESIAN_POINT('',(0.,0.,0.));
#1699=CARTESIAN_POINT('Origin',(0.,0.,0.));
#1700=CARTESIAN_POINT('',(-0.525,0.2,6.4293956955236E-17));
#1701=CARTESIAN_POINT('Origin',(0.,0.2,0.));
#1702=CARTESIAN_POINT('',(-0.525,0.,6.4293956955236E-17));
#1703=CARTESIAN_POINT('',(-0.525,0.,6.4293956955236E-17));
#1704=CARTESIAN_POINT('Origin',(0.,0.,0.));
#1705=CARTESIAN_POINT('Origin',(0.,0.,0.));
#1706=CARTESIAN_POINT('',(-1.,0.2,1.22464679914735E-16));
#1707=CARTESIAN_POINT('Origin',(0.,0.2,0.));
#1708=CARTESIAN_POINT('',(-1.,0.,1.22464679914735E-16));
#1709=CARTESIAN_POINT('',(-1.,0.,1.22464679914735E-16));
#1710=CARTESIAN_POINT('Origin',(0.,0.,0.));
#1711=CARTESIAN_POINT('Origin',(0.,0.2,0.));
#1712=CARTESIAN_POINT('Origin',(0.,0.,0.));
#1815=UNCERTAINTY_MEASURE_WITH_UNIT(LENGTH_MEASURE(0.001),#1830,
'DISTANCE_ACCURACY_VALUE',
'Maximum model space distance between geometric entities at asserted c
onnectivities');
#1817=UNCERTAINTY_MEASURE_WITH_UNIT(LENGTH_MEASURE(0.001),#1830,
'DISTANCE_ACCURACY_VALUE',
'Maximum model space distance between geometric entities at asserted c
onnectivities');
#1827=(
GEOMETRIC_REPRESENTATION_CONTEXT(3)
GLOBAL_UNCERTAINTY_ASSIGNED_CONTEXT((#1815))
GLOBAL_UNIT_ASSIGNED_CONTEXT((#1830,#1832,#1833))
REPRESENTATION_CONTEXT('','3D')
);
#1829=(
GEOMETRIC_REPRESENTATION_CONTEXT(3)
GLOBAL_UNCERTAINTY_ASSIGNED_CONTEXT((#1817))
GLOBAL_UNIT_ASSIGNED_CONTEXT((#1830,#1832,#1833))
REPRESENTATION_CONTEXT('','3D')
);
#1830=(
LENGTH_UNIT()
NAMED_UNIT(*)
SI_UNIT(.CENTI.,.METRE.)
);
#1832=(
NAMED_UNIT(*)
PLANE_ANGLE_UNIT()
SI_UNIT($,.RADIAN.)
);
#1833=(
NAMED_UNIT(*)
SI_UNIT($,.STERADIAN.)
SOLID_ANGLE_UNIT()
);
#1843=SHAPE_DEFINITION_REPRESENTATION(#1858,#1886);
#1858=PRODUCT_DEFINITION_SHAPE('',$,#1898);
#1886=SHAPE_REPRESENTATION('',(#1094),#1827);
#1888=PRODUCT_DEFINITION_CONTEXT('part definition',#1923,'design');
#1898=PRODUCT_DEFINITION('Flat Washer - M10','Flat Washer - M10',#1909,
#1888);
#1909=PRODUCT_DEFINITION_FORMATION('',$,#1934);
#1923=APPLICATION_CONTEXT(
'Core Data for Automotive Mechanical Design Process');
#1924=PRODUCT_CONTEXT('part definition',#1923,'mechanical');
#1934=PRODUCT('Flat Washer - M10','Flat Washer - M10',
'Flat Washer - M10',(#1924));
#1985=COLOUR_RGB('Black',0.12,0.14,0.17);
#1986=FILL_AREA_STYLE_COLOUR('',#1985);
#1987=FILL_AREA_STYLE('',(#1986));
#1988=SURFACE_STYLE_FILL_AREA(#1987);
#1989=SURFACE_SIDE_STYLE('',(#1988));
#1990=SURFACE_STYLE_USAGE(.BOTH.,#1989);
#1991=PRESENTATION_STYLE_ASSIGNMENT((#1990));
ENDSEC;
END-ISO-10303-21;
